ISO-10303-21;
HEADER;
/* Generated by software containing ST-Developer
 * from STEP Tools, Inc. (www.steptools.com) 
 */

FILE_DESCRIPTION(
/* description */ ('Rack and pinion manual slide'),
/* implementation_level */ '2;1');

FILE_NAME(
/* name */ 'M5x14 Cap Screw.step',
/* time_stamp */ '2026-10-28T03:22:49-07:00',
/* author */ (''),
/* organization */ (''),
/* preprocessor_version */ 'ST-DEVELOPER v20.2',
/* originating_system */ 'Autodesk Translation Framework v15.17.0.0',
/* authorisation */ '');

FILE_SCHEMA (('AUTOMOTIVE_DESIGN { 1 0 10303 214 3 1 1 }'));
ENDSEC;

DATA;
#10=MECHANICAL_DESIGN_GEOMETRIC_PRESENTATION_REPRESENTATION('',(#769),#34851);
#607=ORIENTED_CLOSED_SHELL('',*,#13791,.F.);
#612=BREP_WITH_VOIDS('Body1',#13792,(#607));
#627=CONICAL_SURFACE('',#15187,0.4,0.785398163397448);
#628=CONICAL_SURFACE('',#15191,0.41,0.785398163397448);
#629=CONICAL_SURFACE('',#15195,0.26,0.463647609000806);
#670=SHAPE_REPRESENTATION_RELATIONSHIP('SRR','None',#35108,#716);
#716=ADVANCED_BREP_SHAPE_REPRESENTATION('',(#612),#34833);
#769=STYLED_ITEM('',(#35418),#612);
#1009=FACE_BOUND('',#2985,.T.);
#1423=PLANE('',#15175);
#1424=PLANE('',#15176);
#1425=PLANE('',#15177);
#1426=PLANE('',#15178);
#1427=PLANE('',#15179);
#1428=PLANE('',#15180);
#1429=PLANE('',#15181);
#1430=PLANE('',#15182);
#1431=PLANE('',#15183);
#1432=PLANE('',#15185);
#1433=PLANE('',#15193);
#2056=FACE_OUTER_BOUND('',#2971,.T.);
#2057=FACE_OUTER_BOUND('',#2972,.T.);
#2058=FACE_OUTER_BOUND('',#2973,.T.);
#2059=FACE_OUTER_BOUND('',#2974,.T.);
#2060=FACE_OUTER_BOUND('',#2975,.T.);
#2061=FACE_OUTER_BOUND('',#2976,.T.);
#2062=FACE_OUTER_BOUND('',#2977,.T.);
#2063=FACE_OUTER_BOUND('',#2978,.T.);
#2064=FACE_OUTER_BOUND('',#2979,.T.);
#2065=FACE_OUTER_BOUND('',#2980,.T.);
#2066=FACE_OUTER_BOUND('',#2981,.T.);
#2067=FACE_OUTER_BOUND('',#2982,.T.);
#2068=FACE_OUTER_BOUND('',#2983,.T.);
#2069=FACE_OUTER_BOUND('',#2984,.T.);
#2070=FACE_OUTER_BOUND('',#2986,.T.);
#2071=FACE_OUTER_BOUND('',#2987,.T.);
#2971=EDGE_LOOP('',(#11852,#11853,#11854,#11855));
#2972=EDGE_LOOP('',(#11856,#11857,#11858,#11859));
#2973=EDGE_LOOP('',(#11860,#11861,#11862,#11863));
#2974=EDGE_LOOP('',(#11864,#11865,#11866,#11867));
#2975=EDGE_LOOP('',(#11868,#11869,#11870,#11871));
#2976=EDGE_LOOP('',(#11872,#11873,#11874,#11875));
#2977=EDGE_LOOP('',(#11876,#11877,#11878,#11879,#11880,#11881));
#2978=EDGE_LOOP('',(#11882,#11883,#11884,#11885,#11886,#11887));
#2979=EDGE_LOOP('',(#11888));
#2980=EDGE_LOOP('',(#11889));
#2981=EDGE_LOOP('',(#11890,#11891,#11892,#11893));
#2982=EDGE_LOOP('',(#11894,#11895,#11896,#11897));
#2983=EDGE_LOOP('',(#11898,#11899,#11900,#11901));
#2984=EDGE_LOOP('',(#11902));
#2985=EDGE_LOOP('',(#11903));
#2986=EDGE_LOOP('',(#11904,#11905,#11906,#11907));
#2987=EDGE_LOOP('',(#11908,#11909,#11910,#11911));
#4226=LINE('',#22506,#5517);
#4227=LINE('',#22508,#5518);
#4228=LINE('',#22510,#5519);
#4229=LINE('',#22511,#5520);
#4230=LINE('',#22514,#5521);
#4231=LINE('',#22516,#5522);
#4232=LINE('',#22517,#5523);
#4233=LINE('',#22520,#5524);
#4234=LINE('',#22522,#5525);
#4235=LINE('',#22523,#5526);
#4236=LINE('',#22526,#5527);
#4237=LINE('',#22528,#5528);
#4238=LINE('',#22529,#5529);
#4239=LINE('',#22532,#5530);
#4240=LINE('',#22534,#5531);
#4241=LINE('',#22535,#5532);
#4242=LINE('',#22537,#5533);
#4243=LINE('',#22538,#5534);
#4244=LINE('',#22550,#5535);
#4245=LINE('',#22554,#5536);
#4246=LINE('',#22558,#5537);
#4247=LINE('',#22565,#5538);
#4248=LINE('',#22567,#5539);
#5517=VECTOR('',#18320,1.);
#5518=VECTOR('',#18321,1.);
#5519=VECTOR('',#18322,1.);
#5520=VECTOR('',#18323,1.);
#5521=VECTOR('',#18326,1.);
#5522=VECTOR('',#18327,1.);
#5523=VECTOR('',#18328,1.);
#5524=VECTOR('',#18331,1.);
#5525=VECTOR('',#18332,1.);
#5526=VECTOR('',#18333,1.);
#5527=VECTOR('',#18336,1.);
#5528=VECTOR('',#18337,1.);
#5529=VECTOR('',#18338,1.);
#5530=VECTOR('',#18341,1.);
#5531=VECTOR('',#18342,1.);
#5532=VECTOR('',#18343,1.);
#5533=VECTOR('',#18346,1.);
#5534=VECTOR('',#18347,1.);
#5535=VECTOR('',#18364,0.4);
#5536=VECTOR('',#18369,0.425);
#5537=VECTOR('',#18374,0.41);
#5538=VECTOR('',#18383,0.26);
#5539=VECTOR('',#18386,0.25);
#6097=CIRCLE('',#15184,0.24505);
#6098=CIRCLE('',#15186,0.375);
#6099=CIRCLE('',#15188,0.425);
#6100=CIRCLE('',#15190,0.425);
#6101=CIRCLE('',#15192,0.395);
#6102=CIRCLE('',#15194,0.27);
#6103=CIRCLE('',#15196,0.24505);
#7102=VERTEX_POINT('',#22504);
#7103=VERTEX_POINT('',#22505);
#7104=VERTEX_POINT('',#22507);
#7105=VERTEX_POINT('',#22509);
#7106=VERTEX_POINT('',#22513);
#7107=VERTEX_POINT('',#22515);
#7108=VERTEX_POINT('',#22519);
#7109=VERTEX_POINT('',#22521);
#7110=VERTEX_POINT('',#22525);
#7111=VERTEX_POINT('',#22527);
#7112=VERTEX_POINT('',#22531);
#7113=VERTEX_POINT('',#22533);
#7114=VERTEX_POINT('',#22542);
#7115=VERTEX_POINT('',#22545);
#7116=VERTEX_POINT('',#22548);
#7117=VERTEX_POINT('',#22552);
#7118=VERTEX_POINT('',#22556);
#7119=VERTEX_POINT('',#22560);
#7120=VERTEX_POINT('',#22563);
#8738=EDGE_CURVE('',#7102,#7103,#4226,.T.);
#8739=EDGE_CURVE('',#7103,#7104,#4227,.T.);
#8740=EDGE_CURVE('',#7104,#7105,#4228,.T.);
#8741=EDGE_CURVE('',#7102,#7105,#4229,.T.);
#8742=EDGE_CURVE('',#7103,#7106,#4230,.T.);
#8743=EDGE_CURVE('',#7106,#7107,#4231,.T.);
#8744=EDGE_CURVE('',#7107,#7104,#4232,.T.);
#8745=EDGE_CURVE('',#7106,#7108,#4233,.T.);
#8746=EDGE_CURVE('',#7108,#7109,#4234,.T.);
#8747=EDGE_CURVE('',#7109,#7107,#4235,.T.);
#8748=EDGE_CURVE('',#7108,#7110,#4236,.T.);
#8749=EDGE_CURVE('',#7110,#7111,#4237,.T.);
#8750=EDGE_CURVE('',#7111,#7109,#4238,.T.);
#8751=EDGE_CURVE('',#7110,#7112,#4239,.T.);
#8752=EDGE_CURVE('',#7112,#7113,#4240,.T.);
#8753=EDGE_CURVE('',#7113,#7111,#4241,.T.);
#8754=EDGE_CURVE('',#7112,#7102,#4242,.T.);
#8755=EDGE_CURVE('',#7105,#7113,#4243,.T.);
#8756=EDGE_CURVE('',#7114,#7114,#6097,.T.);
#8757=EDGE_CURVE('',#7115,#7115,#6098,.T.);
#8758=EDGE_CURVE('',#7116,#7116,#6099,.T.);
#8759=EDGE_CURVE('',#7116,#7115,#4244,.T.);
#8760=EDGE_CURVE('',#7117,#7117,#6100,.T.);
#8761=EDGE_CURVE('',#7117,#7116,#4245,.T.);
#8762=EDGE_CURVE('',#7118,#7118,#6101,.T.);
#8763=EDGE_CURVE('',#7118,#7117,#4246,.T.);
#8764=EDGE_CURVE('',#7119,#7119,#6102,.T.);
#8765=EDGE_CURVE('',#7120,#7120,#6103,.F.);
#8766=EDGE_CURVE('',#7120,#7119,#4247,.T.);
#8767=EDGE_CURVE('',#7114,#7120,#4248,.T.);
#11852=ORIENTED_EDGE('',*,*,#8738,.T.);
#11853=ORIENTED_EDGE('',*,*,#8739,.T.);
#11854=ORIENTED_EDGE('',*,*,#8740,.T.);
#11855=ORIENTED_EDGE('',*,*,#8741,.F.);
#11856=ORIENTED_EDGE('',*,*,#8742,.T.);
#11857=ORIENTED_EDGE('',*,*,#8743,.T.);
#11858=ORIENTED_EDGE('',*,*,#8744,.T.);
#11859=ORIENTED_EDGE('',*,*,#8739,.F.);
#11860=ORIENTED_EDGE('',*,*,#8745,.T.);
#11861=ORIENTED_EDGE('',*,*,#8746,.T.);
#11862=ORIENTED_EDGE('',*,*,#8747,.T.);
#11863=ORIENTED_EDGE('',*,*,#8743,.F.);
#11864=ORIENTED_EDGE('',*,*,#8748,.T.);
#11865=ORIENTED_EDGE('',*,*,#8749,.T.);
#11866=ORIENTED_EDGE('',*,*,#8750,.T.);
#11867=ORIENTED_EDGE('',*,*,#8746,.F.);
#11868=ORIENTED_EDGE('',*,*,#8751,.T.);
#11869=ORIENTED_EDGE('',*,*,#8752,.T.);
#11870=ORIENTED_EDGE('',*,*,#8753,.T.);
#11871=ORIENTED_EDGE('',*,*,#8749,.F.);
#11872=ORIENTED_EDGE('',*,*,#8754,.T.);
#11873=ORIENTED_EDGE('',*,*,#8741,.T.);
#11874=ORIENTED_EDGE('',*,*,#8755,.T.);
#11875=ORIENTED_EDGE('',*,*,#8752,.F.);
#11876=ORIENTED_EDGE('',*,*,#8754,.F.);
#11877=ORIENTED_EDGE('',*,*,#8751,.F.);
#11878=ORIENTED_EDGE('',*,*,#8748,.F.);
#11879=ORIENTED_EDGE('',*,*,#8745,.F.);
#11880=ORIENTED_EDGE('',*,*,#8742,.F.);
#11881=ORIENTED_EDGE('',*,*,#8738,.F.);
#11882=ORIENTED_EDGE('',*,*,#8755,.F.);
#11883=ORIENTED_EDGE('',*,*,#8740,.F.);
#11884=ORIENTED_EDGE('',*,*,#8744,.F.);
#11885=ORIENTED_EDGE('',*,*,#8747,.F.);
#11886=ORIENTED_EDGE('',*,*,#8750,.F.);
#11887=ORIENTED_EDGE('',*,*,#8753,.F.);
#11888=ORIENTED_EDGE('',*,*,#8756,.F.);
#11889=ORIENTED_EDGE('',*,*,#8757,.F.);
#11890=ORIENTED_EDGE('',*,*,#8758,.F.);
#11891=ORIENTED_EDGE('',*,*,#8759,.T.);
#11892=ORIENTED_EDGE('',*,*,#8757,.T.);
#11893=ORIENTED_EDGE('',*,*,#8759,.F.);
#11894=ORIENTED_EDGE('',*,*,#8760,.F.);
#11895=ORIENTED_EDGE('',*,*,#8761,.T.);
#11896=ORIENTED_EDGE('',*,*,#8758,.T.);
#11897=ORIENTED_EDGE('',*,*,#8761,.F.);
#11898=ORIENTED_EDGE('',*,*,#8762,.F.);
#11899=ORIENTED_EDGE('',*,*,#8763,.T.);
#11900=ORIENTED_EDGE('',*,*,#8760,.T.);
#11901=ORIENTED_EDGE('',*,*,#8763,.F.);
#11902=ORIENTED_EDGE('',*,*,#8762,.T.);
#11903=ORIENTED_EDGE('',*,*,#8764,.F.);
#11904=ORIENTED_EDGE('',*,*,#8765,.F.);
#11905=ORIENTED_EDGE('',*,*,#8766,.T.);
#11906=ORIENTED_EDGE('',*,*,#8764,.T.);
#11907=ORIENTED_EDGE('',*,*,#8766,.F.);
#11908=ORIENTED_EDGE('',*,*,#8756,.T.);
#11909=ORIENTED_EDGE('',*,*,#8767,.T.);
#11910=ORIENTED_EDGE('',*,*,#8765,.T.);
#11911=ORIENTED_EDGE('',*,*,#8767,.F.);
#12958=CYLINDRICAL_SURFACE('',#15189,0.425);
#12959=CYLINDRICAL_SURFACE('',#15197,0.24505);
#13534=ADVANCED_FACE('',(#2056),#1423,.F.);
#13535=ADVANCED_FACE('',(#2057),#1424,.F.);
#13536=ADVANCED_FACE('',(#2058),#1425,.F.);
#13537=ADVANCED_FACE('',(#2059),#1426,.F.);
#13538=ADVANCED_FACE('',(#2060),#1427,.F.);
#13539=ADVANCED_FACE('',(#2061),#1428,.F.);
#13540=ADVANCED_FACE('',(#2062),#1429,.F.);
#13541=ADVANCED_FACE('',(#2063),#1430,.F.);
#13542=ADVANCED_FACE('',(#2064),#1431,.F.);
#13543=ADVANCED_FACE('',(#2065),#1432,.T.);
#13544=ADVANCED_FACE('',(#2066),#627,.T.);
#13545=ADVANCED_FACE('',(#2067),#12958,.T.);
#13546=ADVANCED_FACE('',(#2068),#628,.T.);
#13547=ADVANCED_FACE('',(#2069,#1009),#1433,.T.);
#13548=ADVANCED_FACE('',(#2070),#629,.T.);
#13549=ADVANCED_FACE('',(#2071),#12959,.T.);
#13791=CLOSED_SHELL('',(#13534,#13535,#13536,#13537,#13538,#13539,#13540,
#13541));
#13792=CLOSED_SHELL('',(#13542,#13543,#13544,#13545,#13546,#13547,#13548,
#13549));
#15174=AXIS2_PLACEMENT_3D('',#22502,#18316,#18317);
#15175=AXIS2_PLACEMENT_3D('',#22503,#18318,#18319);
#15176=AXIS2_PLACEMENT_3D('',#22512,#18324,#18325);
#15177=AXIS2_PLACEMENT_3D('',#22518,#18329,#18330);
#15178=AXIS2_PLACEMENT_3D('',#22524,#18334,#18335);
#15179=AXIS2_PLACEMENT_3D('',#22530,#18339,#18340);
#15180=AXIS2_PLACEMENT_3D('',#22536,#18344,#18345);
#15181=AXIS2_PLACEMENT_3D('',#22539,#18348,#18349);
#15182=AXIS2_PLACEMENT_3D('',#22540,#18350,#18351);
#15183=AXIS2_PLACEMENT_3D('',#22541,#18352,#18353);
#15184=AXIS2_PLACEMENT_3D('',#22543,#18354,#18355);
#15185=AXIS2_PLACEMENT_3D('',#22544,#18356,#18357);
#15186=AXIS2_PLACEMENT_3D('',#22546,#18358,#18359);
#15187=AXIS2_PLACEMENT_3D('',#22547,#18360,#18361);
#15188=AXIS2_PLACEMENT_3D('',#22549,#18362,#18363);
#15189=AXIS2_PLACEMENT_3D('',#22551,#18365,#18366);
#15190=AXIS2_PLACEMENT_3D('',#22553,#18367,#18368);
#15191=AXIS2_PLACEMENT_3D('',#22555,#18370,#18371);
#15192=AXIS2_PLACEMENT_3D('',#22557,#18372,#18373);
#15193=AXIS2_PLACEMENT_3D('',#22559,#18375,#18376);
#15194=AXIS2_PLACEMENT_3D('',#22561,#18377,#18378);
#15195=AXIS2_PLACEMENT_3D('',#22562,#18379,#18380);
#15196=AXIS2_PLACEMENT_3D('',#22564,#18381,#18382);
#15197=AXIS2_PLACEMENT_3D('',#22566,#18384,#18385);
#18316=DIRECTION('axis',(0.,0.,1.));
#18317=DIRECTION('refdir',(1.,0.,0.));
#18318=DIRECTION('center_axis',(0.866025403784439,0.,-0.5));
#18319=DIRECTION('ref_axis',(0.5,0.,0.866025403784439));
#18320=DIRECTION('',(-0.5,0.,-0.866025403784439));
#18321=DIRECTION('',(0.,-1.,0.));
#18322=DIRECTION('',(0.5,0.,0.866025403784439));
#18323=DIRECTION('',(0.,-1.,0.));
#18324=DIRECTION('center_axis',(1.20185167898973E-16,0.,-1.));
#18325=DIRECTION('ref_axis',(1.,0.,1.20185167898973E-16));
#18326=DIRECTION('',(-1.,0.,-1.20185167898973E-16));
#18327=DIRECTION('',(0.,-1.,0.));
#18328=DIRECTION('',(1.,0.,1.20185167898973E-16));
#18329=DIRECTION('center_axis',(-0.866025403784439,0.,-0.5));
#18330=DIRECTION('ref_axis',(0.5,0.,-0.866025403784439));
#18331=DIRECTION('',(-0.5,0.,0.866025403784439));
#18332=DIRECTION('',(0.,-1.,0.));
#18333=DIRECTION('',(0.5,0.,-0.866025403784439));
#18334=DIRECTION('center_axis',(-0.866025403784439,0.,0.5));
#18335=DIRECTION('ref_axis',(-0.5,0.,-0.866025403784439));
#18336=DIRECTION('',(0.5,0.,0.866025403784439));
#18337=DIRECTION('',(0.,-1.,0.));
#18338=DIRECTION('',(-0.5,0.,-0.866025403784439));
#18339=DIRECTION('center_axis',(-2.40370335797945E-16,0.,1.));
#18340=DIRECTION('ref_axis',(-1.,0.,-2.40370335797945E-16));
#18341=DIRECTION('',(1.,0.,2.40370335797945E-16));
#18342=DIRECTION('',(0.,-1.,0.));
#18343=DIRECTION('',(-1.,0.,-2.40370335797945E-16));
#18344=DIRECTION('center_axis',(0.866025403784439,0.,0.5));
#18345=DIRECTION('ref_axis',(-0.5,0.,0.866025403784439));
#18346=DIRECTION('',(0.5,0.,-0.866025403784439));
#18347=DIRECTION('',(-0.5,0.,0.866025403784439));
#18348=DIRECTION('center_axis',(0.,1.,0.));
#18349=DIRECTION('ref_axis',(1.,0.,0.));
#18350=DIRECTION('center_axis',(0.,-1.,0.));
#18351=DIRECTION('ref_axis',(0.,0.,-1.));
#18352=DIRECTION('center_axis',(0.,1.,0.));
#18353=DIRECTION('ref_axis',(1.,0.,0.));
#18354=DIRECTION('center_axis',(0.,1.,0.));
#18355=DIRECTION('ref_axis',(1.,0.,0.));
#18356=DIRECTION('center_axis',(0.,1.,0.));
#18357=DIRECTION('ref_axis',(0.,0.,1.));
#18358=DIRECTION('center_axis',(0.,-1.,0.));
#18359=DIRECTION('ref_axis',(1.,0.,0.));
#18360=DIRECTION('center_axis',(0.,-1.,0.));
#18361=DIRECTION('ref_axis',(1.,0.,0.));
#18362=DIRECTION('center_axis',(0.,-1.,0.));
#18363=DIRECTION('ref_axis',(1.,0.,0.));
#18364=DIRECTION('',(0.707106781186548,0.707106781186547,8.65956056235493E-17));
#18365=DIRECTION('center_axis',(0.,-1.,0.));
#18366=DIRECTION('ref_axis',(1.,0.,0.));
#18367=DIRECTION('center_axis',(0.,-1.,0.));
#18368=DIRECTION('ref_axis',(1.,0.,0.));
#18369=DIRECTION('',(0.,1.,0.));
#18370=DIRECTION('center_axis',(0.,1.,0.));
#18371=DIRECTION('ref_axis',(1.,0.,0.));
#18372=DIRECTION('center_axis',(0.,-1.,0.));
#18373=DIRECTION('ref_axis',(1.,0.,0.));
#18374=DIRECTION('',(-0.707106781186547,0.707106781186548,-8.65956056235493E-17));
#18375=DIRECTION('center_axis',(0.,-1.,0.));
#18376=DIRECTION('ref_axis',(0.,0.,-1.));
#18377=DIRECTION('center_axis',(0.,-1.,0.));
#18378=DIRECTION('ref_axis',(1.,0.,0.));
#18379=DIRECTION('center_axis',(0.,1.,0.));
#18380=DIRECTION('ref_axis',(1.,0.,0.));
#18381=DIRECTION('center_axis',(0.,1.,0.));
#18382=DIRECTION('ref_axis',(1.,0.,0.));
#18383=DIRECTION('',(-0.447213595499958,0.894427190999916,-5.47678698264203E-17));
#18384=DIRECTION('center_axis',(0.,-1.,0.));
#18385=DIRECTION('ref_axis',(1.,0.,0.));
#18386=DIRECTION('',(0.,1.,0.));
#22502=CARTESIAN_POINT('',(0.,0.,0.));
#22503=CARTESIAN_POINT('Origin',(0.115470053837925,-0.5,-0.2));
#22504=CARTESIAN_POINT('',(0.23094010767585,-0.5,0.));
#22505=CARTESIAN_POINT('',(0.115470053837925,-0.5,-0.2));
#22506=CARTESIAN_POINT('',(0.23094010767585,-0.5,0.));
#22507=CARTESIAN_POINT('',(0.115470053837925,-0.8,-0.2));
#22508=CARTESIAN_POINT('',(0.115470053837925,-0.5,-0.2));
#22509=CARTESIAN_POINT('',(0.23094010767585,-0.8,0.));
#22510=CARTESIAN_POINT('',(0.23094010767585,-0.8,0.));
#22511=CARTESIAN_POINT('',(0.23094010767585,-0.5,0.));
#22512=CARTESIAN_POINT('Origin',(-0.115470053837925,-0.5,-0.2));
#22513=CARTESIAN_POINT('',(-0.115470053837925,-0.5,-0.2));
#22514=CARTESIAN_POINT('',(0.115470053837925,-0.5,-0.2));
#22515=CARTESIAN_POINT('',(-0.115470053837925,-0.8,-0.2));
#22516=CARTESIAN_POINT('',(-0.115470053837925,-0.5,-0.2));
#22517=CARTESIAN_POINT('',(0.115470053837925,-0.8,-0.2));
#22518=CARTESIAN_POINT('Origin',(-0.23094010767585,-0.5,-2.77555756156289E-17));
#22519=CARTESIAN_POINT('',(-0.23094010767585,-0.5,-2.82820063659975E-17));
#22520=CARTESIAN_POINT('',(-0.115470053837925,-0.5,-0.2));
#22521=CARTESIAN_POINT('',(-0.23094010767585,-0.8,-2.77555756156289E-17));
#22522=CARTESIAN_POINT('',(-0.23094010767585,-0.5,-2.82820063659975E-17));
#22523=CARTESIAN_POINT('',(-0.115470053837925,-0.8,-0.2));
#22524=CARTESIAN_POINT('Origin',(-0.115470053837925,-0.5,0.2));
#22525=CARTESIAN_POINT('',(-0.115470053837925,-0.5,0.2));
#22526=CARTESIAN_POINT('',(-0.23094010767585,-0.5,-2.82820063659975E-17));
#22527=CARTESIAN_POINT('',(-0.115470053837925,-0.8,0.2));
#22528=CARTESIAN_POINT('',(-0.115470053837925,-0.5,0.2));
#22529=CARTESIAN_POINT('',(-0.23094010767585,-0.8,-2.82820063659975E-17));
#22530=CARTESIAN_POINT('Origin',(0.115470053837925,-0.5,0.2));
#22531=CARTESIAN_POINT('',(0.115470053837925,-0.5,0.2));
#22532=CARTESIAN_POINT('',(-0.115470053837925,-0.5,0.2));
#22533=CARTESIAN_POINT('',(0.115470053837925,-0.8,0.2));
#22534=CARTESIAN_POINT('',(0.115470053837925,-0.5,0.2));
#22535=CARTESIAN_POINT('',(-0.115470053837925,-0.8,0.2));
#22536=CARTESIAN_POINT('Origin',(0.23094010767585,-0.5,0.));
#22537=CARTESIAN_POINT('',(0.115470053837925,-0.5,0.2));
#22538=CARTESIAN_POINT('',(0.115470053837925,-0.8,0.2));
#22539=CARTESIAN_POINT('Origin',(0.,-0.5,0.));
#22540=CARTESIAN_POINT('Origin',(0.,-0.8,0.));
#22541=CARTESIAN_POINT('Origin',(0.,-1.4,0.));
#22542=CARTESIAN_POINT('',(-0.24505,-1.4,3.00099698131059E-17));
#22543=CARTESIAN_POINT('Origin',(0.,-1.4,0.));
#22544=CARTESIAN_POINT('Origin',(0.375,0.5,0.));
#22545=CARTESIAN_POINT('',(-0.375,0.5,-4.59242549680257E-17));
#22546=CARTESIAN_POINT('Origin',(0.,0.5,0.));
#22547=CARTESIAN_POINT('Origin',(0.,0.475,0.));
#22548=CARTESIAN_POINT('',(-0.425,0.45,-5.20474889637625E-17));
#22549=CARTESIAN_POINT('Origin',(0.,0.45,0.));
#22550=CARTESIAN_POINT('',(-0.4,0.475,-4.89858719658941E-17));
#22551=CARTESIAN_POINT('Origin',(0.,0.24,0.));
#22552=CARTESIAN_POINT('',(-0.425,0.0299999999999998,-5.20474889637625E-17));
#22553=CARTESIAN_POINT('Origin',(0.,0.0299999999999998,0.));
#22554=CARTESIAN_POINT('',(-0.425,0.24,-5.20474889637625E-17));
#22555=CARTESIAN_POINT('Origin',(0.,0.0150000000000001,0.));
#22556=CARTESIAN_POINT('',(-0.395,4.85722573273506E-17,-4.83735485663204E-17));
#22557=CARTESIAN_POINT('Origin',(0.,0.,0.));
#22558=CARTESIAN_POINT('',(-0.41,0.0150000000000001,-5.02105187650415E-17));
#22559=CARTESIAN_POINT('Origin',(0.27,0.,0.));
#22560=CARTESIAN_POINT('',(-0.27,0.,-3.30654635769785E-17));
#22561=CARTESIAN_POINT('Origin',(0.,0.,0.));
#22562=CARTESIAN_POINT('Origin',(0.,-0.02,0.));
#22563=CARTESIAN_POINT('',(-0.24505,-0.0498999999999999,3.00099698131059E-17));
#22564=CARTESIAN_POINT('Origin',(0.,-0.0498999999999999,0.));
#22565=CARTESIAN_POINT('',(-0.26,-0.02,-3.18408167778312E-17));
#22566=CARTESIAN_POINT('Origin',(0.,-0.995,0.));
#22567=CARTESIAN_POINT('',(-0.24505,-0.995,-3.00099698131059E-17));
#34779=UNCERTAINTY_MEASURE_WITH_UNIT(LENGTH_MEASURE(0.001),#34852,
'DISTANCE_ACCURACY_VALUE',
'Maximum model space distance between geometric entities at asserted c
onnectivities');
#34797=UNCERTAINTY_MEASURE_WITH_UNIT(LENGTH_MEASURE(0.001),#34852,
'DISTANCE_ACCURACY_VALUE',
'Maximum model space distance between geometric entities at asserted c
onnectivities');
#34833=(
GEOMETRIC_REPRESENTATION_CONTEXT(3)
GLOBAL_UNCERTAINTY_ASSIGNED_CONTEXT((#34779))
GLOBAL_UNIT_ASSIGNED_CONTEXT((#34852,#34854,#34855))
REPRESENTATION_CONTEXT('','3D')
);
#34851=(
GEOMETRIC_REPRESENTATION_CONTEXT(3)
GLOBAL_UNCERTAINTY_ASSIGNED_CONTEXT((#34797))
GLOBAL_UNIT_ASSIGNED_CONTEXT((#34852,#34854,#34855))
REPRESENTATION_CONTEXT('','3D')
);
#34852=(
LENGTH_UNIT()
NAMED_UNIT(*)
SI_UNIT(.CENTI.,.METRE.)
);
#34854=(
NAMED_UNIT(*)
PLANE_ANGLE_UNIT()
SI_UNIT($,.RADIAN.)
);
#34855=(
NAMED_UNIT(*)
SI_UNIT($,.STERADIAN.)
SOLID_ANGLE_UNIT()
);
#34891=SHAPE_DEFINITION_REPRESENTATION(#34952,#35108);
#34952=PRODUCT_DEFINITION_SHAPE('',$,#35162);
#35108=SHAPE_REPRESENTATION('',(#15174),#34833);
#35126=PRODUCT_DEFINITION_CONTEXT('part definition',#35287,'design');
#35162=PRODUCT_DEFINITION('M5x14 Cap Screw','M5x14 Cap Screw',#35215,#35126);
#35215=PRODUCT_DEFINITION_FORMATION('',$,#35324);
#35287=APPLICATION_CONTEXT(
'Core Data for Automotive Mechanical Design Process');
#35288=PRODUCT_CONTEXT('part definition',#35287,'mechanical');
#35324=PRODUCT('M5x14 Cap Screw','M5x14 Cap Screw','M5x14 Cap Screw',(#35288));
#35412=COLOUR_RGB('Black',0.12,0.14,0.17);
#35413=FILL_AREA_STYLE_COLOUR('',#35412);
#35414=FILL_AREA_STYLE('',(#35413));
#35415=SURFACE_STYLE_FILL_AREA(#35414);
#35416=SURFACE_SIDE_STYLE('',(#35415));
#35417=SURFACE_STYLE_USAGE(.BOTH.,#35416);
#35418=PRESENTATION_STYLE_ASSIGNMENT((#35417));
ENDSEC;
END-ISO-10303-21;
